ISO-10303-21;
HEADER;
/* Generated by software containing ST-Developer
 * from STEP Tools, Inc. (www.steptools.com) 
 */

FILE_DESCRIPTION(
/* description */ (''),
/* implementation_level */ '2;1');

FILE_NAME(
/* name */ 'Middle_Part_02.step',
/* time_stamp */ '2026-10-06T13:23:02-07:00',
/* author */ (''),
/* organization */ (''),
/* preprocessor_version */ 'ST-DEVELOPER v20.2',
/* originating_system */ 'Autodesk Translation Framework v15.15.0.0',
/* authorisation */ '');

FILE_SCHEMA (('AUTOMOTIVE_DESIGN { 1 0 10303 214 3 1 1 }'));
ENDSEC;

DATA;
#10=MECHANICAL_DESIGN_GEOMETRIC_PRESENTATION_REPRESENTATION('',(#77),#4994);
#57=SHAPE_REPRESENTATION_RELATIONSHIP('SRR','None',#5038,#67);
#67=ADVANCED_BREP_SHAPE_REPRESENTATION('',(#87),#4990);
#77=STYLED_ITEM('',(#5093),#87);
#87=MANIFOLD_SOLID_BREP('Body1',#2917);
#115=CYLINDRICAL_SURFACE('',#3235,1.);
#116=CYLINDRICAL_SURFACE('',#3238,1.);
#150=FACE_BOUND('',#649,.T.);
#151=FACE_BOUND('',#650,.T.);
#152=FACE_BOUND('',#652,.T.);
#153=FACE_BOUND('',#653,.T.);
#259=PLANE('',#3241);
#260=PLANE('',#3242);
#261=PLANE('',#3243);
#262=PLANE('',#3244);
#263=PLANE('',#3245);
#264=PLANE('',#3246);
#265=PLANE('',#3247);
#266=PLANE('',#3248);
#267=PLANE('',#3249);
#268=PLANE('',#3250);
#433=FACE_OUTER_BOUND('',#638,.T.);
#434=FACE_OUTER_BOUND('',#639,.T.);
#435=FACE_OUTER_BOUND('',#640,.T.);
#436=FACE_OUTER_BOUND('',#641,.T.);
#437=FACE_OUTER_BOUND('',#642,.T.);
#438=FACE_OUTER_BOUND('',#643,.T.);
#439=FACE_OUTER_BOUND('',#644,.T.);
#440=FACE_OUTER_BOUND('',#645,.T.);
#441=FACE_OUTER_BOUND('',#646,.T.);
#442=FACE_OUTER_BOUND('',#647,.T.);
#443=FACE_OUTER_BOUND('',#648,.T.);
#444=FACE_OUTER_BOUND('',#651,.T.);
#638=EDGE_LOOP('',(#2484,#2485,#2486,#2487));
#639=EDGE_LOOP('',(#2488,#2489,#2490,#2491));
#640=EDGE_LOOP('',(#2492,#2493,#2494,#2495));
#641=EDGE_LOOP('',(#2496,#2497,#2498,#2499));
#642=EDGE_LOOP('',(#2500,#2501,#2502,#2503));
#643=EDGE_LOOP('',(#2504,#2505,#2506,#2507));
#644=EDGE_LOOP('',(#2508,#2509,#2510,#2511));
#645=EDGE_LOOP('',(#2512,#2513,#2514,#2515));
#646=EDGE_LOOP('',(#2516,#2517,#2518,#2519));
#647=EDGE_LOOP('',(#2520,#2521,#2522,#2523));
#648=EDGE_LOOP('',(#2524,#2525,#2526,#2527,#2528,#2529,#2530,#2531));
#649=EDGE_LOOP('',(#2532));
#650=EDGE_LOOP('',(#2533));
#651=EDGE_LOOP('',(#2534,#2535,#2536,#2537,#2538,#2539,#2540,#2541));
#652=EDGE_LOOP('',(#2542));
#653=EDGE_LOOP('',(#2543));
#891=LINE('',#4714,#1184);
#892=LINE('',#4720,#1185);
#893=LINE('',#4725,#1186);
#894=LINE('',#4727,#1187);
#895=LINE('',#4729,#1188);
#896=LINE('',#4730,#1189);
#897=LINE('',#4733,#1190);
#898=LINE('',#4735,#1191);
#899=LINE('',#4736,#1192);
#900=LINE('',#4739,#1193);
#901=LINE('',#4741,#1194);
#902=LINE('',#4742,#1195);
#903=LINE('',#4745,#1196);
#904=LINE('',#4747,#1197);
#905=LINE('',#4748,#1198);
#906=LINE('',#4751,#1199);
#907=LINE('',#4753,#1200);
#908=LINE('',#4754,#1201);
#909=LINE('',#4757,#1202);
#910=LINE('',#4759,#1203);
#911=LINE('',#4760,#1204);
#912=LINE('',#4763,#1205);
#913=LINE('',#4765,#1206);
#914=LINE('',#4766,#1207);
#915=LINE('',#4768,#1208);
#916=LINE('',#4769,#1209);
#1184=VECTOR('',#3911,1.);
#1185=VECTOR('',#3918,1.);
#1186=VECTOR('',#3923,10.);
#1187=VECTOR('',#3924,10.);
#1188=VECTOR('',#3925,10.);
#1189=VECTOR('',#3926,10.);
#1190=VECTOR('',#3929,10.);
#1191=VECTOR('',#3930,10.);
#1192=VECTOR('',#3931,10.);
#1193=VECTOR('',#3934,10.);
#1194=VECTOR('',#3935,10.);
#1195=VECTOR('',#3936,10.);
#1196=VECTOR('',#3939,10.);
#1197=VECTOR('',#3940,10.);
#1198=VECTOR('',#3941,10.);
#1199=VECTOR('',#3944,10.);
#1200=VECTOR('',#3945,10.);
#1201=VECTOR('',#3946,10.);
#1202=VECTOR('',#3949,10.);
#1203=VECTOR('',#3950,10.);
#1204=VECTOR('',#3951,10.);
#1205=VECTOR('',#3954,10.);
#1206=VECTOR('',#3955,10.);
#1207=VECTOR('',#3956,10.);
#1208=VECTOR('',#3959,10.);
#1209=VECTOR('',#3960,10.);
#1353=CIRCLE('',#3236,1.);
#1354=CIRCLE('',#3237,1.);
#1355=CIRCLE('',#3239,1.);
#1356=CIRCLE('',#3240,1.);
#1522=VERTEX_POINT('',#4711);
#1523=VERTEX_POINT('',#4713);
#1524=VERTEX_POINT('',#4717);
#1525=VERTEX_POINT('',#4719);
#1526=VERTEX_POINT('',#4723);
#1527=VERTEX_POINT('',#4724);
#1528=VERTEX_POINT('',#4726);
#1529=VERTEX_POINT('',#4728);
#1530=VERTEX_POINT('',#4732);
#1531=VERTEX_POINT('',#4734);
#1532=VERTEX_POINT('',#4738);
#1533=VERTEX_POINT('',#4740);
#1534=VERTEX_POINT('',#4744);
#1535=VERTEX_POINT('',#4746);
#1536=VERTEX_POINT('',#4750);
#1537=VERTEX_POINT('',#4752);
#1538=VERTEX_POINT('',#4756);
#1539=VERTEX_POINT('',#4758);
#1540=VERTEX_POINT('',#4762);
#1541=VERTEX_POINT('',#4764);
#1856=EDGE_CURVE('',#1522,#1522,#1353,.T.);
#1857=EDGE_CURVE('',#1522,#1523,#891,.T.);
#1858=EDGE_CURVE('',#1523,#1523,#1354,.T.);
#1859=EDGE_CURVE('',#1524,#1524,#1355,.T.);
#1860=EDGE_CURVE('',#1524,#1525,#892,.T.);
#1861=EDGE_CURVE('',#1525,#1525,#1356,.T.);
#1862=EDGE_CURVE('',#1526,#1527,#893,.T.);
#1863=EDGE_CURVE('',#1526,#1528,#894,.T.);
#1864=EDGE_CURVE('',#1528,#1529,#895,.T.);
#1865=EDGE_CURVE('',#1527,#1529,#896,.T.);
#1866=EDGE_CURVE('',#1530,#1526,#897,.T.);
#1867=EDGE_CURVE('',#1530,#1531,#898,.T.);
#1868=EDGE_CURVE('',#1531,#1528,#899,.T.);
#1869=EDGE_CURVE('',#1532,#1530,#900,.T.);
#1870=EDGE_CURVE('',#1532,#1533,#901,.T.);
#1871=EDGE_CURVE('',#1533,#1531,#902,.T.);
#1872=EDGE_CURVE('',#1534,#1532,#903,.T.);
#1873=EDGE_CURVE('',#1534,#1535,#904,.T.);
#1874=EDGE_CURVE('',#1535,#1533,#905,.T.);
#1875=EDGE_CURVE('',#1536,#1534,#906,.T.);
#1876=EDGE_CURVE('',#1536,#1537,#907,.T.);
#1877=EDGE_CURVE('',#1537,#1535,#908,.T.);
#1878=EDGE_CURVE('',#1538,#1536,#909,.T.);
#1879=EDGE_CURVE('',#1538,#1539,#910,.T.);
#1880=EDGE_CURVE('',#1539,#1537,#911,.T.);
#1881=EDGE_CURVE('',#1540,#1538,#912,.T.);
#1882=EDGE_CURVE('',#1540,#1541,#913,.T.);
#1883=EDGE_CURVE('',#1541,#1539,#914,.T.);
#1884=EDGE_CURVE('',#1527,#1540,#915,.T.);
#1885=EDGE_CURVE('',#1529,#1541,#916,.T.);
#2484=ORIENTED_EDGE('',*,*,#1856,.T.);
#2485=ORIENTED_EDGE('',*,*,#1857,.T.);
#2486=ORIENTED_EDGE('',*,*,#1858,.T.);
#2487=ORIENTED_EDGE('',*,*,#1857,.F.);
#2488=ORIENTED_EDGE('',*,*,#1859,.T.);
#2489=ORIENTED_EDGE('',*,*,#1860,.T.);
#2490=ORIENTED_EDGE('',*,*,#1861,.T.);
#2491=ORIENTED_EDGE('',*,*,#1860,.F.);
#2492=ORIENTED_EDGE('',*,*,#1862,.F.);
#2493=ORIENTED_EDGE('',*,*,#1863,.T.);
#2494=ORIENTED_EDGE('',*,*,#1864,.T.);
#2495=ORIENTED_EDGE('',*,*,#1865,.F.);
#2496=ORIENTED_EDGE('',*,*,#1866,.F.);
#2497=ORIENTED_EDGE('',*,*,#1867,.T.);
#2498=ORIENTED_EDGE('',*,*,#1868,.T.);
#2499=ORIENTED_EDGE('',*,*,#1863,.F.);
#2500=ORIENTED_EDGE('',*,*,#1869,.F.);
#2501=ORIENTED_EDGE('',*,*,#1870,.T.);
#2502=ORIENTED_EDGE('',*,*,#1871,.T.);
#2503=ORIENTED_EDGE('',*,*,#1867,.F.);
#2504=ORIENTED_EDGE('',*,*,#1872,.F.);
#2505=ORIENTED_EDGE('',*,*,#1873,.T.);
#2506=ORIENTED_EDGE('',*,*,#1874,.T.);
#2507=ORIENTED_EDGE('',*,*,#1870,.F.);
#2508=ORIENTED_EDGE('',*,*,#1875,.F.);
#2509=ORIENTED_EDGE('',*,*,#1876,.T.);
#2510=ORIENTED_EDGE('',*,*,#1877,.T.);
#2511=ORIENTED_EDGE('',*,*,#1873,.F.);
#2512=ORIENTED_EDGE('',*,*,#1878,.F.);
#2513=ORIENTED_EDGE('',*,*,#1879,.T.);
#2514=ORIENTED_EDGE('',*,*,#1880,.T.);
#2515=ORIENTED_EDGE('',*,*,#1876,.F.);
#2516=ORIENTED_EDGE('',*,*,#1881,.F.);
#2517=ORIENTED_EDGE('',*,*,#1882,.T.);
#2518=ORIENTED_EDGE('',*,*,#1883,.T.);
#2519=ORIENTED_EDGE('',*,*,#1879,.F.);
#2520=ORIENTED_EDGE('',*,*,#1884,.F.);
#2521=ORIENTED_EDGE('',*,*,#1865,.T.);
#2522=ORIENTED_EDGE('',*,*,#1885,.T.);
#2523=ORIENTED_EDGE('',*,*,#1882,.F.);
#2524=ORIENTED_EDGE('',*,*,#1885,.F.);
#2525=ORIENTED_EDGE('',*,*,#1864,.F.);
#2526=ORIENTED_EDGE('',*,*,#1868,.F.);
#2527=ORIENTED_EDGE('',*,*,#1871,.F.);
#2528=ORIENTED_EDGE('',*,*,#1874,.F.);
#2529=ORIENTED_EDGE('',*,*,#1877,.F.);
#2530=ORIENTED_EDGE('',*,*,#1880,.F.);
#2531=ORIENTED_EDGE('',*,*,#1883,.F.);
#2532=ORIENTED_EDGE('',*,*,#1858,.F.);
#2533=ORIENTED_EDGE('',*,*,#1861,.F.);
#2534=ORIENTED_EDGE('',*,*,#1884,.T.);
#2535=ORIENTED_EDGE('',*,*,#1881,.T.);
#2536=ORIENTED_EDGE('',*,*,#1878,.T.);
#2537=ORIENTED_EDGE('',*,*,#1875,.T.);
#2538=ORIENTED_EDGE('',*,*,#1872,.T.);
#2539=ORIENTED_EDGE('',*,*,#1869,.T.);
#2540=ORIENTED_EDGE('',*,*,#1866,.T.);
#2541=ORIENTED_EDGE('',*,*,#1862,.T.);
#2542=ORIENTED_EDGE('',*,*,#1856,.F.);
#2543=ORIENTED_EDGE('',*,*,#1859,.F.);
#2863=ADVANCED_FACE('',(#433),#115,.F.);
#2864=ADVANCED_FACE('',(#434),#116,.F.);
#2865=ADVANCED_FACE('',(#435),#259,.F.);
#2866=ADVANCED_FACE('',(#436),#260,.F.);
#2867=ADVANCED_FACE('',(#437),#261,.F.);
#2868=ADVANCED_FACE('',(#438),#262,.F.);
#2869=ADVANCED_FACE('',(#439),#263,.F.);
#2870=ADVANCED_FACE('',(#440),#264,.F.);
#2871=ADVANCED_FACE('',(#441),#265,.F.);
#2872=ADVANCED_FACE('',(#442),#266,.F.);
#2873=ADVANCED_FACE('',(#443,#150,#151),#267,.F.);
#2874=ADVANCED_FACE('',(#444,#152,#153),#268,.T.);
#2917=CLOSED_SHELL('',(#2863,#2864,#2865,#2866,#2867,#2868,#2869,#2870,
#2871,#2872,#2873,#2874));
#3234=AXIS2_PLACEMENT_3D('',#4709,#3905,#3906);
#3235=AXIS2_PLACEMENT_3D('',#4710,#3907,#3908);
#3236=AXIS2_PLACEMENT_3D('',#4712,#3909,#3910);
#3237=AXIS2_PLACEMENT_3D('',#4715,#3912,#3913);
#3238=AXIS2_PLACEMENT_3D('',#4716,#3914,#3915);
#3239=AXIS2_PLACEMENT_3D('',#4718,#3916,#3917);
#3240=AXIS2_PLACEMENT_3D('',#4721,#3919,#3920);
#3241=AXIS2_PLACEMENT_3D('',#4722,#3921,#3922);
#3242=AXIS2_PLACEMENT_3D('',#4731,#3927,#3928);
#3243=AXIS2_PLACEMENT_3D('',#4737,#3932,#3933);
#3244=AXIS2_PLACEMENT_3D('',#4743,#3937,#3938);
#3245=AXIS2_PLACEMENT_3D('',#4749,#3942,#3943);
#3246=AXIS2_PLACEMENT_3D('',#4755,#3947,#3948);
#3247=AXIS2_PLACEMENT_3D('',#4761,#3952,#3953);
#3248=AXIS2_PLACEMENT_3D('',#4767,#3957,#3958);
#3249=AXIS2_PLACEMENT_3D('',#4770,#3961,#3962);
#3250=AXIS2_PLACEMENT_3D('',#4771,#3963,#3964);
#3905=DIRECTION('axis',(0.,0.,1.));
#3906=DIRECTION('refdir',(1.,0.,0.));
#3907=DIRECTION('center_axis',(-1.,0.,0.));
#3908=DIRECTION('ref_axis',(0.,1.,0.));
#3909=DIRECTION('center_axis',(1.,0.,0.));
#3910=DIRECTION('ref_axis',(0.,1.,0.));
#3911=DIRECTION('',(-1.,0.,0.));
#3912=DIRECTION('center_axis',(-1.,0.,0.));
#3913=DIRECTION('ref_axis',(0.,1.,0.));
#3914=DIRECTION('center_axis',(-1.,0.,0.));
#3915=DIRECTION('ref_axis',(0.,1.,0.));
#3916=DIRECTION('center_axis',(1.,0.,0.));
#3917=DIRECTION('ref_axis',(0.,1.,0.));
#3918=DIRECTION('',(-1.,0.,0.));
#3919=DIRECTION('center_axis',(-1.,0.,0.));
#3920=DIRECTION('ref_axis',(0.,1.,0.));
#3921=DIRECTION('center_axis',(0.,0.,-1.));
#3922=DIRECTION('ref_axis',(0.,-1.,0.));
#3923=DIRECTION('',(0.,-1.,0.));
#3924=DIRECTION('',(-1.,0.,0.));
#3925=DIRECTION('',(0.,-1.,0.));
#3926=DIRECTION('',(-1.,0.,0.));
#3927=DIRECTION('center_axis',(0.,-1.,0.));
#3928=DIRECTION('ref_axis',(0.,0.,1.));
#3929=DIRECTION('',(0.,0.,1.));
#3930=DIRECTION('',(-1.,0.,0.));
#3931=DIRECTION('',(0.,0.,1.));
#3932=DIRECTION('center_axis',(0.,0.,1.));
#3933=DIRECTION('ref_axis',(0.,1.,0.));
#3934=DIRECTION('',(0.,1.,0.));
#3935=DIRECTION('',(-1.,0.,0.));
#3936=DIRECTION('',(0.,1.,0.));
#3937=DIRECTION('center_axis',(0.,1.,0.));
#3938=DIRECTION('ref_axis',(0.,0.,-1.));
#3939=DIRECTION('',(0.,0.,-1.));
#3940=DIRECTION('',(-1.,0.,0.));
#3941=DIRECTION('',(0.,0.,-1.));
#3942=DIRECTION('center_axis',(0.,0.,1.));
#3943=DIRECTION('ref_axis',(0.,1.,0.));
#3944=DIRECTION('',(0.,1.,0.));
#3945=DIRECTION('',(-1.,0.,0.));
#3946=DIRECTION('',(0.,1.,0.));
#3947=DIRECTION('center_axis',(0.,-1.,1.24327477962315E-16));
#3948=DIRECTION('ref_axis',(0.,1.24327477962315E-16,1.));
#3949=DIRECTION('',(0.,1.24327477962315E-16,1.));
#3950=DIRECTION('',(-1.,0.,0.));
#3951=DIRECTION('',(0.,1.24327477962315E-16,1.));
#3952=DIRECTION('center_axis',(0.,0.,1.));
#3953=DIRECTION('ref_axis',(0.,1.,0.));
#3954=DIRECTION('',(0.,1.,0.));
#3955=DIRECTION('',(-1.,0.,0.));
#3956=DIRECTION('',(0.,1.,0.));
#3957=DIRECTION('center_axis',(0.,1.,0.));
#3958=DIRECTION('ref_axis',(0.,0.,-1.));
#3959=DIRECTION('',(0.,0.,-1.));
#3960=DIRECTION('',(0.,0.,-1.));
#3961=DIRECTION('center_axis',(1.,0.,0.));
#3962=DIRECTION('ref_axis',(0.,0.,-1.));
#3963=DIRECTION('center_axis',(1.,0.,0.));
#3964=DIRECTION('ref_axis',(0.,1.,0.));
#4709=CARTESIAN_POINT('',(0.,0.,0.));
#4710=CARTESIAN_POINT('Origin',(-14.5,7.24395366693103,1.75498192028357));
#4711=CARTESIAN_POINT('',(-9.5,6.24395366693103,1.75498192028357));
#4712=CARTESIAN_POINT('Origin',(-9.5,7.24395366693103,1.75498192028357));
#4713=CARTESIAN_POINT('',(-13.5,6.24395366693103,1.75498192028357));
#4714=CARTESIAN_POINT('',(-14.5,6.24395366693103,1.75498192028357));
#4715=CARTESIAN_POINT('Origin',(-13.5,7.24395366693103,1.75498192028357));
#4716=CARTESIAN_POINT('Origin',(-14.5,-7.24395366693103,1.75498192028357));
#4717=CARTESIAN_POINT('',(-9.5,-8.24395366693103,1.75498192028357));
#4718=CARTESIAN_POINT('Origin',(-9.5,-7.24395366693103,1.75498192028357));
#4719=CARTESIAN_POINT('',(-13.5,-8.24395366693103,1.75498192028357));
#4720=CARTESIAN_POINT('',(-14.5,-8.24395366693103,1.75498192028357));
#4721=CARTESIAN_POINT('Origin',(-13.5,-7.24395366693103,1.75498192028357));
#4722=CARTESIAN_POINT('Origin',(-9.5,10.0039433906299,6.26348125396711));
#4723=CARTESIAN_POINT('',(-9.5,10.0039433906299,6.26348125396711));
#4724=CARTESIAN_POINT('',(-9.5,-10.0039433906299,6.26348125396711));
#4725=CARTESIAN_POINT('',(-9.5,10.0039433906299,6.26348125396711));
#4726=CARTESIAN_POINT('',(-13.5,10.0039433906299,6.26348125396711));
#4727=CARTESIAN_POINT('',(-9.5,10.0039433906299,6.26348125396711));
#4728=CARTESIAN_POINT('',(-13.5,-10.0039433906299,6.26348125396711));
#4729=CARTESIAN_POINT('',(-13.5,10.0039433906299,6.26348125396711));
#4730=CARTESIAN_POINT('',(-9.5,-10.0039433906299,6.26348125396711));
#4731=CARTESIAN_POINT('Origin',(-9.5,10.0039433906299,-1.2346845122375));
#4732=CARTESIAN_POINT('',(-9.5,10.0039433906299,-1.2346845122375));
#4733=CARTESIAN_POINT('',(-9.5,10.0039433906299,-1.2346845122375));
#4734=CARTESIAN_POINT('',(-13.5,10.0039433906299,-1.2346845122375));
#4735=CARTESIAN_POINT('',(-9.5,10.0039433906299,-1.2346845122375));
#4736=CARTESIAN_POINT('',(-13.5,10.0039433906299,-1.2346845122375));
#4737=CARTESIAN_POINT('Origin',(-9.5,4.48396394323217,-1.2346845122375));
#4738=CARTESIAN_POINT('',(-9.5,4.48396394323217,-1.2346845122375));
#4739=CARTESIAN_POINT('',(-9.5,-10.0039433906299,-1.2346845122375));
#4740=CARTESIAN_POINT('',(-13.5,4.48396394323217,-1.2346845122375));
#4741=CARTESIAN_POINT('',(-9.5,4.48396394323217,-1.2346845122375));
#4742=CARTESIAN_POINT('',(-13.5,-10.0039433906299,-1.2346845122375));
#4743=CARTESIAN_POINT('Origin',(-9.5,4.48396394323217,3.23022961141938));
#4744=CARTESIAN_POINT('',(-9.5,4.48396394323217,3.23022961141938));
#4745=CARTESIAN_POINT('',(-9.5,4.48396394323217,3.23022961141938));
#4746=CARTESIAN_POINT('',(-13.5,4.48396394323217,3.23022961141938));
#4747=CARTESIAN_POINT('',(-9.5,4.48396394323217,3.23022961141938));
#4748=CARTESIAN_POINT('',(-13.5,4.48396394323217,3.23022961141938));
#4749=CARTESIAN_POINT('Origin',(-9.5,-4.48396394323217,3.23022961141938));
#4750=CARTESIAN_POINT('',(-9.5,-4.48396394323217,3.23022961141938));
#4751=CARTESIAN_POINT('',(-9.5,-4.48396394323217,3.23022961141938));
#4752=CARTESIAN_POINT('',(-13.5,-4.48396394323217,3.23022961141938));
#4753=CARTESIAN_POINT('',(-9.5,-4.48396394323217,3.23022961141938));
#4754=CARTESIAN_POINT('',(-13.5,-4.48396394323217,3.23022961141938));
#4755=CARTESIAN_POINT('Origin',(-9.5,-4.48396394323217,-1.2346845122375));
#4756=CARTESIAN_POINT('',(-9.5,-4.48396394323217,-1.2346845122375));
#4757=CARTESIAN_POINT('',(-9.5,-4.48396394323217,-1.2346845122375));
#4758=CARTESIAN_POINT('',(-13.5,-4.48396394323217,-1.2346845122375));
#4759=CARTESIAN_POINT('',(-9.5,-4.48396394323217,-1.2346845122375));
#4760=CARTESIAN_POINT('',(-13.5,-4.48396394323217,-1.2346845122375));
#4761=CARTESIAN_POINT('Origin',(-9.5,-10.0039433906299,-1.2346845122375));
#4762=CARTESIAN_POINT('',(-9.5,-10.0039433906299,-1.2346845122375));
#4763=CARTESIAN_POINT('',(-9.5,-10.0039433906299,-1.2346845122375));
#4764=CARTESIAN_POINT('',(-13.5,-10.0039433906299,-1.2346845122375));
#4765=CARTESIAN_POINT('',(-9.5,-10.0039433906299,-1.2346845122375));
#4766=CARTESIAN_POINT('',(-13.5,-10.0039433906299,-1.2346845122375));
#4767=CARTESIAN_POINT('Origin',(-9.5,-10.0039433906299,6.26348125396711));
#4768=CARTESIAN_POINT('',(-9.5,-10.0039433906299,6.26348125396711));
#4769=CARTESIAN_POINT('',(-13.5,-10.0039433906299,6.26348125396711));
#4770=CARTESIAN_POINT('Origin',(-13.5,0.,2.51439837086481));
#4771=CARTESIAN_POINT('Origin',(-9.5,0.,2.51439837086481));
#4978=UNCERTAINTY_MEASURE_WITH_UNIT(LENGTH_MEASURE(0.01),#4995,
'DISTANCE_ACCURACY_VALUE',
'Maximum model space distance between geometric entities at asserted c
onnectivities');
#4982=UNCERTAINTY_MEASURE_WITH_UNIT(LENGTH_MEASURE(0.01),#4995,
'DISTANCE_ACCURACY_VALUE',
'Maximum model space distance between geometric entities at asserted c
onnectivities');
#4990=(
GEOMETRIC_REPRESENTATION_CONTEXT(3)
GLOBAL_UNCERTAINTY_ASSIGNED_CONTEXT((#4978))
GLOBAL_UNIT_ASSIGNED_CONTEXT((#4995,#4997,#4998))
REPRESENTATION_CONTEXT('','3D')
);
#4994=(
GEOMETRIC_REPRESENTATION_CONTEXT(3)
GLOBAL_UNCERTAINTY_ASSIGNED_CONTEXT((#4982))
GLOBAL_UNIT_ASSIGNED_CONTEXT((#4995,#4997,#4998))
REPRESENTATION_CONTEXT('','3D')
);
#4995=(
LENGTH_UNIT()
NAMED_UNIT(*)
SI_UNIT(.MILLI.,.METRE.)
);
#4997=(
NAMED_UNIT(*)
PLANE_ANGLE_UNIT()
SI_UNIT($,.RADIAN.)
);
#4998=(
NAMED_UNIT(*)
SI_UNIT($,.STERADIAN.)
SOLID_ANGLE_UNIT()
);
#5006=SHAPE_DEFINITION_REPRESENTATION(#5017,#5038);
#5017=PRODUCT_DEFINITION_SHAPE('',$,#5050);
#5038=SHAPE_REPRESENTATION('',(#3234),#4990);
#5042=PRODUCT_DEFINITION_CONTEXT('part definition',#5077,'design');
#5050=PRODUCT_DEFINITION('Middle_Part_02','Middle_Part_02',#5061,#5042);
#5061=PRODUCT_DEFINITION_FORMATION('',$,#5086);
#5077=APPLICATION_CONTEXT(
'Core Data for Automotive Mechanical Design Process');
#5078=PRODUCT_CONTEXT('part definition',#5077,'mechanical');
#5086=PRODUCT('Middle_Part_02','Middle_Part_02',$,(#5078));
#5093=PRESENTATION_STYLE_ASSIGNMENT((#5098));
#5098=SURFACE_STYLE_USAGE(.BOTH.,#5103);
#5103=SURFACE_SIDE_STYLE('',(#5108));
#5108=SURFACE_STYLE_FILL_AREA(#5113);
#5113=FILL_AREA_STYLE('Opaque(70,70,209)',(#5118));
#5118=FILL_AREA_STYLE_COLOUR('Opaque(70,70,209)',#5123);
#5123=COLOUR_RGB('Opaque(70,70,209)', 0.09019608, 0.27058824, 0.51372549);
ENDSEC;
END-ISO-10303-21;
